ISO-10303-21;
HEADER;
FILE_DESCRIPTION (('STEP AP214'),
    '1' );
FILE_NAME ('Screw 1.step',
    '2026-10-26T17:37:43',
    ( '' ),
    ( '' ),
    'SwSTEP 2.0',
    'SolidWorks 2024',
    '' );
FILE_SCHEMA (( 'AUTOMOTIVE_DESIGN' ));
ENDSEC;

DATA;
#27=( NAMED_UNIT ( * ) SI_UNIT ( $, .STERADIAN. ) SOLID_ANGLE_UNIT ( ) );
#69=AXIS2_PLACEMENT_3D ( 'NONE', #21536, #19655, #7123 ) ;
#70=DIRECTION ( 'NONE',  ( -1.000000000000000000, 2.330758767201999921E-14, 2.343004830739999973E-14 ) ) ;
#77=EDGE_LOOP ( 'NONE', ( #5442, #11222, #19525, #6801 ) ) ;
#144=CARTESIAN_POINT ( 'NONE',  ( -12.69999999999999929, -3577.293829546999859, 2244.679313203000220 ) ) ;
#174=CARTESIAN_POINT ( 'NONE',  ( -8.890000000008001280, -3580.206200000000081, 2249.723686796999573 ) ) ;
#199=DIRECTION ( 'NONE',  ( -1.000000000000000000, -3.885294924352999876E-13, 3.885294924352999876E-13 ) ) ;
#263=DIRECTION ( 'NONE',  ( -2.343004830739999973E-14, -1.784212334590129905E-30, -1.000000000000000000 ) ) ;
#292=DIRECTION ( 'NONE',  ( -1.000000000000000000, 2.318894227180000040E-14, 2.343004830739999973E-14 ) ) ;
#329=EDGE_LOOP ( 'NONE', ( #8854, #6013, #22023, #18423, #7464, #6906 ) ) ;
#335=ORIENTED_EDGE ( 'NONE', *, *, #8776, .F. ) ;
#339=DIRECTION ( 'NONE',  ( 0.000000000000000000, -1.165588477296860248E-12, 1.000000000000000000 ) ) ;
#351=EDGE_CURVE ( 'NONE', #22087, #15975, #10618, .T. ) ;
#406=DIRECTION ( 'NONE',  ( 0.000000000000000000, -0.8660254037825031448, -0.5000000000033524294 ) ) ;
#563=DIRECTION ( 'NONE',  ( 1.000000000000000000, 0.000000000000000000, 0.000000000000000000 ) ) ;
#571=AXIS2_PLACEMENT_3D ( 'NONE', #16730, #14869, #10564 ) ;
#595=AXIS2_PLACEMENT_3D ( 'NONE', #12987, #7589, #14400 ) ;
#625=ORIENTED_EDGE ( 'NONE', *, *, #3214, .F. ) ;
#715=CARTESIAN_POINT ( 'NONE',  ( -12.31900000000001505, -3577.513799999857383, 2249.723686796824950 ) ) ;
#729=DIRECTION ( 'NONE',  ( 0.000000000000000000, -1.000000000000000000, 0.000000000000000000 ) ) ;
#746=EDGE_CURVE ( 'NONE', #18142, #1451, #22119, .T. ) ;
#758=EDGE_LOOP ( 'NONE', ( #7533, #4820 ) ) ;
#840=DIRECTION ( 'NONE',  ( 0.000000000000000000, -1.000000000000000000, 0.000000000000000000 ) ) ;
#863=DIRECTION ( 'NONE',  ( 2.216404975961944229E-13, 0.5000000000040877302, 0.8660254037820787065 ) ) ;
#887=AXIS2_PLACEMENT_3D ( 'NONE', #10637, #19084, #12172 ) ;
#913=ADVANCED_FACE ( 'NONE', ( #5567 ), #3673, .T. ) ;
#973=ORIENTED_EDGE ( 'NONE', *, *, #14428, .F. ) ;
#979=CIRCLE ( 'NONE', #16695, 0.3809999999999993947 ) ;
#1011=CYLINDRICAL_SURFACE ( 'NONE', #18913, 3.175000000000149925 ) ;
#1016=ORIENTED_EDGE ( 'NONE', *, *, #14533, .F. ) ;
#1030=DIRECTION ( 'NONE',  ( -1.000000000000000000, 1.295098308110999804E-13, 2.590196616220999964E-13 ) ) ;
#1050=DIRECTION ( 'NONE',  ( 0.000000000000000000, -1.000000000000000000, 0.000000000000000000 ) ) ;
#1065=EDGE_CURVE ( 'NONE', #15615, #6279, #20636, .T. ) ;
#1114=ADVANCED_FACE ( 'NONE', ( #4472 ), #22052, .T. ) ;
#1115=CARTESIAN_POINT ( 'NONE',  ( -12.69999999999997087, -3577.293829547214045, 2250.104686797002159 ) ) ;
#1146=ORIENTED_EDGE ( 'NONE', *, *, #19120, .T. ) ;
#1160=CARTESIAN_POINT ( 'NONE',  ( -6.349999999999999645, -3578.860000000000127, 2247.392000000000280 ) ) ;
#1174=DIRECTION ( 'NONE',  ( -1.000000000000000000, 0.000000000000000000, 0.000000000000000000 ) ) ;
#1243=ORIENTED_EDGE ( 'NONE', *, *, #16662, .T. ) ;
#1267=DIRECTION ( 'NONE',  ( 0.000000000000000000, 0.000000000000000000, 1.000000000000000000 ) ) ;
#1298=VECTOR ( 'NONE', #9093, 1000.000000000000000 ) ;
#1330=AXIS2_PLACEMENT_3D ( 'NONE', #5129, #4880, #7115 ) ;
#1383=AXIS2_PLACEMENT_3D ( 'NONE', #7175, #5419, #6343 ) ;
#1398=VERTEX_POINT ( 'NONE', #18287 ) ;
#1450=DIRECTION ( 'NONE',  ( 1.000000000000000000, 0.000000000000000000, 0.000000000000000000 ) ) ;
#1451=VERTEX_POINT ( 'NONE', #4450 ) ;
#1497=VECTOR ( 'NONE', #13193, 1000.000000000000114 ) ;
#1532=CARTESIAN_POINT ( 'NONE',  ( -12.31899999999987827, -3576.167599999831964, 2247.391999999993914 ) ) ;
#1553=DIRECTION ( 'NONE',  ( 0.000000000000000000, -1.000000000000000000, 0.000000000000000000 ) ) ;
#1557=EDGE_CURVE ( 'NONE', #8915, #6279, #4988, .T. ) ;
#1606=DIRECTION ( 'NONE',  ( -1.000000000000000000, 0.000000000000000000, -1.295098308109999907E-13 ) ) ;
#1643=DIRECTION ( 'NONE',  ( 4.703417536272999698E-14, 1.000000000000000000, 2.474126484833999786E-12 ) ) ;
#1659=( NAMED_UNIT ( * ) PLANE_ANGLE_UNIT ( ) SI_UNIT ( $, .RADIAN. ) );
#1715=VERTEX_POINT ( 'NONE', #23062 ) ;
#1782=EDGE_LOOP ( 'NONE', ( #15963, #16432 ) ) ;
#1915=CARTESIAN_POINT ( 'NONE',  ( -12.31900000000000084, -3576.167599999999766, 2247.392000000000280 ) ) ;
#1916=EDGE_LOOP ( 'NONE', ( #12690, #14299, #22719, #12758, #21325, #19968 ) ) ;
#1936=CYLINDRICAL_SURFACE ( 'NONE', #10928, 0.3810000000000746678 ) ;
#2052=CARTESIAN_POINT ( 'NONE',  ( -12.31900000000000084, -3581.209255678999853, 2246.035656601000028 ) ) ;
#2102=VERTEX_POINT ( 'NONE', #22799 ) ;
#2206=ORIENTED_EDGE ( 'NONE', *, *, #16409, .T. ) ;
#2257=( GEOMETRIC_REPRESENTATION_CONTEXT ( 3 ) GLOBAL_UNCERTAINTY_ASSIGNED_CONTEXT ( ( #16741 ) ) GLOBAL_UNIT_ASSIGNED_CONTEXT ( ( #21126, #3419, #23094 ) ) REPRESENTATION_CONTEXT ( 'NONE', 'WORKASPACE' ) );
#2260=EDGE_CURVE ( 'NONE', #8915, #2597, #3592, .T. ) ;
#2266=ORIENTED_EDGE ( 'NONE', *, *, #12866, .F. ) ;
#2313=LINE ( 'NONE', #11434, #1497 ) ;
#2333=DIRECTION ( 'NONE',  ( 0.000000000000000000, -0.5000000000005969669, 0.8660254037840939834 ) ) ;
#2365=DIRECTION ( 'NONE',  ( -2.356218894535439317E-14, 0.000000000000000000, -1.000000000000000000 ) ) ;
#2370=CARTESIAN_POINT ( 'NONE',  ( -12.70000000000008455, -3580.426170452909901, 2244.679313203224865 ) ) ;
#2385=EDGE_LOOP ( 'NONE', ( #13367, #13612, #3782, #5739 ) ) ;
#2434=VECTOR ( 'NONE', #1174, 1000.000000000000000 ) ;
#2473=ORIENTED_EDGE ( 'NONE', *, *, #6301, .F. ) ;
#2493=CARTESIAN_POINT ( 'NONE',  ( -12.69999999998383977, -3580.297314745246695, 2249.881502164247649 ) ) ;
#2520=CIRCLE ( 'NONE', #20856, 0.3810000000000002829 ) ;
#2572=CARTESIAN_POINT ( 'NONE',  ( -12.31900000000000084, -3578.860000000000127, 2247.392000000000280 ) ) ;
#2581=DIRECTION ( 'NONE',  ( -3.101339145306999912E-14, -1.000000000000000000, -1.984857052996999759E-12 ) ) ;
#2597=VERTEX_POINT ( 'NONE', #3302 ) ;
#2606=CARTESIAN_POINT ( 'NONE',  ( 0.000000000000000000, 0.000000000000000000, 0.000000000000000000 ) ) ;
#2627=DIRECTION ( 'NONE',  ( -2.318894227180156550E-14, -1.000000000000000000, 0.000000000000000000 ) ) ;
#2662=EDGE_CURVE ( 'NONE', #12473, #13851, #5546, .T. ) ;
#2740=LINE ( 'NONE', #18795, #10256 ) ;
#2758=VERTEX_POINT ( 'NONE', #14328 ) ;
#2768=EDGE_CURVE ( 'NONE', #21577, #18508, #8503, .T. ) ;
#2779=CARTESIAN_POINT ( 'NONE',  ( -8.890000000022000748, -3580.206200000000081, 2245.060313203000078 ) ) ;
#2803=CARTESIAN_POINT ( 'NONE',  ( -12.69999999999997087, -3577.293829547214045, 2250.104686797002159 ) ) ;
#2822=CARTESIAN_POINT ( 'NONE',  ( -12.54218463272304085, -3580.206200000483932, 2249.723686796998663 ) ) ;
#2823=EDGE_CURVE ( 'NONE', #12697, #2102, #8098, .T. ) ;
#2828=ORIENTED_EDGE ( 'NONE', *, *, #3971, .F. ) ;
#2838=AXIS2_PLACEMENT_3D ( 'NONE', #3323, #3210, #1450 ) ;
#2842=PRODUCT_CONTEXT ( 'NONE', #7664, 'mechanical' ) ;
#2856=EDGE_CURVE ( 'NONE', #12473, #19963, #14905, .T. ) ;
#2859=DIRECTION ( 'NONE',  ( 0.000000000000000000, -0.5000000000002102762, 0.8660254037843172492 ) ) ;
#2866=AXIS2_PLACEMENT_3D ( 'NONE', #15221, #20957, #22352 ) ;
#2883=CYLINDRICAL_SURFACE ( 'NONE', #13446, 5.460999999999938126 ) ;
#2896=EDGE_CURVE ( 'NONE', #1398, #12697, #7863, .T. ) ;
#3004=ORIENTED_EDGE ( 'NONE', *, *, #19432, .T. ) ;
#3030=DIRECTION ( 'NONE',  ( -1.000000000000000000, 0.000000000000000000, 0.000000000000000000 ) ) ;
#3056=LINE ( 'NONE', #11965, #2434 ) ;
#3076=DIRECTION ( 'NONE',  ( -1.000000000000000000, 0.000000000000000000, 0.000000000000000000 ) ) ;
#3118=PLANE ( 'NONE',  #19315 ) ;
#3146=CARTESIAN_POINT ( 'NONE',  ( -12.31900000000000084, -3576.510744320999947, 2246.035656601000028 ) ) ;
#3210=DIRECTION ( 'NONE',  ( -2.330758767202000237E-14, -1.000000000000000000, -1.224646799141892318E-16 ) ) ;
#3214=EDGE_CURVE ( 'NONE', #7868, #8256, #6533, .T. ) ;
#3251=AXIS2_PLACEMENT_3D ( 'NONE', #12888, #5756, #21794 ) ;
#3269=EDGE_CURVE ( 'NONE', #21296, #13145, #13200, .T. ) ;
#3292=CARTESIAN_POINT ( 'NONE',  ( -12.54218463257233118, -3576.167599999590948, 2247.391999999993914 ) ) ;
#3302=CARTESIAN_POINT ( 'NONE',  ( -12.31900000000000084, -3580.206200000121044, 2249.723686796789480 ) ) ;
#3304=( LENGTH_UNIT ( ) NAMED_UNIT ( * ) SI_UNIT ( .MILLI., .METRE. ) );
#3323=CARTESIAN_POINT ( 'NONE',  ( -12.31899999999988005, -3578.860000000000127, 2252.472000000000207 ) ) ;
#3328=CIRCLE ( 'NONE', #15686, 5.460999999999938126 ) ;
#3376=DIRECTION ( 'NONE',  ( -1.000000000000000000, 2.330758767201999921E-14, 2.343004830739999973E-14 ) ) ;
#3419=( NAMED_UNIT ( * ) PLANE_ANGLE_UNIT ( ) SI_UNIT ( $, .RADIAN. ) );
#3481=VECTOR ( 'NONE', #14074, 1000.000000000000000 ) ;
#3498=CARTESIAN_POINT ( 'NONE',  ( -12.31900000000000084, -3578.860000000000127, 2250.104686796999886 ) ) ;
#3588=VECTOR ( 'NONE', #1643, 1000.000000000000000 ) ;
#3592=LINE ( 'NONE', #10747, #13559 ) ;
#3605=VERTEX_POINT ( 'NONE', #18224 ) ;
#3631=AXIS2_PLACEMENT_3D ( 'NONE', #21475, #13136, #9733 ) ;
#3653=DIRECTION ( 'NONE',  ( 0.000000000000000000, 1.000000000000000000, 0.000000000000000000 ) ) ;
#3673=PLANE ( 'NONE',  #21747 ) ;
#3679=ADVANCED_FACE ( 'NONE', ( #8821 ), #8517, .T. ) ;
#3748=ORIENTED_EDGE ( 'NONE', *, *, #17860, .T. ) ;
#3764=CIRCLE ( 'NONE', #15753, 3.175000000000149925 ) ;
#3777=EDGE_LOOP ( 'NONE', ( #17426, #1243, #4158, #15338, #19915, #17145 ) ) ;
#3782=ORIENTED_EDGE ( 'NONE', *, *, #14019, .F. ) ;
#3824=CARTESIAN_POINT ( 'NONE',  ( -8.890000000017000303, -3577.513800000000174, 2249.723686796999573 ) ) ;
#3971=EDGE_CURVE ( 'NONE', #17006, #12726, #8899, .T. ) ;
#3973=EDGE_CURVE ( 'NONE', #21577, #3605, #2520, .T. ) ;
#4002=DIRECTION ( 'NONE',  ( 3.433625482341074198E-14, 0.5000000000047110094, 0.8660254037817188832 ) ) ;
#4003=EDGE_CURVE ( 'NONE', #8533, #3605, #5534, .T. ) ;
#4013=CARTESIAN_POINT ( 'NONE',  ( -12.31900000000002748, -3580.206200000138779, 2245.060313203175610 ) ) ;
#4073=ORIENTED_EDGE ( 'NONE', *, *, #22008, .F. ) ;
#4133=AXIS2_PLACEMENT_3D ( 'NONE', #9348, #16485, #21989 ) ;
#4158=ORIENTED_EDGE ( 'NONE', *, *, #12957, .F. ) ;
#4201=DIRECTION ( 'NONE',  ( -3.370353031811000117E-12, 1.000000000000000000, 1.649417656554999944E-12 ) ) ;
#4276=DIRECTION ( 'NONE',  ( 0.000000000000000000, -0.8660254037817188832, 0.5000000000047110094 ) ) ;
#4304=DIRECTION ( 'NONE',  ( 5.155718784295149174E-12, -0.5000000000033149039, 0.8660254037825247941 ) ) ;
#4307=TOROIDAL_SURFACE ( 'NONE', #7307, 5.080000000000000071, 0.3810000000000000053 ) ;
#4311=DIRECTION ( 'NONE',  ( 0.000000000000000000, 1.000000000000000000, 0.000000000000000000 ) ) ;
#4312=CARTESIAN_POINT ( 'NONE',  ( 19.05000000000000071, -3578.860000000000127, 2247.392000000000280 ) ) ;
#4343=CARTESIAN_POINT ( 'NONE',  ( -12.69999999993336282, -3577.422685254774024, 2249.881502164204903 ) ) ;
#4346=CARTESIAN_POINT ( 'NONE',  ( -12.69999999999999929, -3577.293829546999859, 2244.679313203000220 ) ) ;
#4366=ORIENTED_EDGE ( 'NONE', *, *, #6966, .F. ) ;
#4372=ORIENTED_EDGE ( 'NONE', *, *, #12695, .T. ) ;
#4375=DIRECTION ( 'NONE',  ( -1.000000000000000000, 0.000000000000000000, 0.000000000000000000 ) ) ;
#4377=CIRCLE ( 'NONE', #2866, 1.904999999999823501 ) ;
#4386=VECTOR ( 'NONE', #22835, 1000.000000000000114 ) ;
#4450=CARTESIAN_POINT ( 'NONE',  ( -12.31900000000012696, -3584.320999999999913, 2247.392000000000280 ) ) ;
#4456=CARTESIAN_POINT ( 'NONE',  ( 19.05000000000000071, -3575.684999999999945, 2247.392000000000280 ) ) ;
#4472=FACE_OUTER_BOUND ( 'NONE', #1916, .T. ) ;
#4531=FACE_OUTER_BOUND ( 'NONE', #11288, .T. ) ;
#4537=VECTOR ( 'NONE', #17008, 1000.000000000000000 ) ;
#4564=( BOUNDED_CURVE ( )  B_SPLINE_CURVE ( 3, ( #22848, #6820, #3292, #1532 ),
 .UNSPECIFIED., .F., .F. ) 
 B_SPLINE_CURVE_WITH_KNOTS ( ( 4, 4 ),
 ( 1.570796327718551932, 3.141592653590084883 ),
 .UNSPECIFIED. ) 
 CURVE ( )  GEOMETRIC_REPRESENTATION_ITEM ( )  RATIONAL_B_SPLINE_CURVE ( ( 1.000000000000000000, 0.8047378543420038444, 0.8047378543420038444, 1.000000000000000000 ) ) 
 REPRESENTATION_ITEM ( '' )  );
#4611=ORIENTED_EDGE ( 'NONE', *, *, #3214, .T. ) ;
#4624=CARTESIAN_POINT ( 'NONE',  ( -8.890000000017000303, -3577.513800000000174, 2249.723686796999573 ) ) ;
#4644=CARTESIAN_POINT ( 'NONE',  ( -12.69999999999999929, -3577.293829546977122, 2244.679313203000220 ) ) ;
#4655=EDGE_CURVE ( 'NONE', #7929, #18142, #22820, .T. ) ;
#4677=EDGE_CURVE ( 'NONE', #22087, #14878, #8246, .T. ) ;
#4726=EDGE_CURVE ( 'NONE', #2597, #19144, #2313, .T. ) ;
#4739=CARTESIAN_POINT ( 'NONE',  ( -8.890000000008999592, -3581.552400000000034, 2247.392000000000280 ) ) ;
#4767=CARTESIAN_POINT ( 'NONE',  ( 19.05000000000000071, -3578.860000000000127, 2247.392000000000280 ) ) ;
#4809=CARTESIAN_POINT ( 'NONE',  ( -6.731000000000118888, -3578.860000000000127, 2242.311999999999898 ) ) ;
#4813=LINE ( 'NONE', #8800, #3588 ) ;
#4820=ORIENTED_EDGE ( 'NONE', *, *, #8642, .T. ) ;
#4880=DIRECTION ( 'NONE',  ( -0.000000000000000000, 0.8660254037825932949, 0.5000000000031962211 ) ) ;
#4901=CARTESIAN_POINT ( 'NONE',  ( -6.730999999999999872, -3578.860000000000127, 2247.392000000000280 ) ) ;
#4913=ADVANCED_FACE ( 'NONE', ( #13661 ), #2883, .T. ) ;
#4945=VERTEX_POINT ( 'NONE', #20564 ) ;
#4988=( BOUNDED_CURVE ( )  B_SPLINE_CURVE ( 3, ( #11704, #18862, #4343, #2803 ),
 .UNSPECIFIED., .F., .T. ) 
 B_SPLINE_CURVE_WITH_KNOTS ( ( 4, 4 ),
 ( 4.051959034059917173E-16, 1.570796326496385786 ),
 .UNSPECIFIED. ) 
 CURVE ( )  GEOMETRIC_REPRESENTATION_ITEM ( )  RATIONAL_B_SPLINE_CURVE ( ( 1.000000000000000000, 0.8047378541947246555, 0.8047378541947246555, 1.000000000000000000 ) ) 
 REPRESENTATION_ITEM ( '' )  );
#5003=CLOSED_SHELL ( 'NONE', ( #12373, #21420, #19860, #4913, #3679, #18468, #5593, #15454, #21466, #20327, #21249, #913, #11676, #19978, #9153, #22176, #11266, #16929, #18419, #11961, #1114, #13604, #6350, #9646, #20187, #19755 ) ) ;
#5006=CARTESIAN_POINT ( 'NONE',  ( -12.31900000000000084, -3577.513799999878302, 2245.060313203211081 ) ) ;
#5109=VECTOR ( 'NONE', #2581, 1000.000000000000000 ) ;
#5128=CARTESIAN_POINT ( 'NONE',  ( -6.730999999999999872, -3578.860000000000127, 2247.392000000000280 ) ) ;
#5129=CARTESIAN_POINT ( 'NONE',  ( -8.890000000004999237, -3581.552400000000034, 2247.392000000000280 ) ) ;
#5136=ORIENTED_EDGE ( 'NONE', *, *, #2768, .F. ) ;
#5154=CARTESIAN_POINT ( 'NONE',  ( -12.70000000000008455, -3580.426170452909901, 2244.679313203224865 ) ) ;
#5180=CARTESIAN_POINT ( 'NONE',  ( -8.890000000026999416, -3576.167599999999766, 2247.392000000000280 ) ) ;
#5204=ORIENTED_EDGE ( 'NONE', *, *, #351, .F. ) ;
#5252=LINE ( 'NONE', #20954, #18045 ) ;
#5295=PLANE ( 'NONE',  #571 ) ;
#5348=CARTESIAN_POINT ( 'NONE',  ( 19.05000000000000071, -3575.684999999999945, 2247.392000000000280 ) ) ;
#5356=DIRECTION ( 'NONE',  ( -3.599768650750962257E-14, -0.5000000000038942183, -0.8660254037821902839 ) ) ;
#5375=AXIS2_PLACEMENT_3D ( 'NONE', #11511, #4375, #729 ) ;
#5409=VERTEX_POINT ( 'NONE', #11013 ) ;
#5418=VECTOR ( 'NONE', #2859, 1000.000000000000000 ) ;
#5419=DIRECTION ( 'NONE',  ( 1.000000000000000000, -2.330758767201999921E-14, -2.339144844575000061E-14 ) ) ;
#5421=AXIS2_PLACEMENT_3D ( 'NONE', #8149, #22080, #6160 ) ;
#5442=ORIENTED_EDGE ( 'NONE', *, *, #2662, .F. ) ;
#5451=CARTESIAN_POINT ( 'NONE',  ( -8.890000000026999416, -3576.167599999999766, 2247.392000000000280 ) ) ;
#5476=AXIS2_PLACEMENT_3D ( 'NONE', #6908, #14053, #17669 ) ;
#5484=DIRECTION ( 'NONE',  ( 1.000000000000000000, -2.334777064353000131E-14, -2.343004830739999973E-14 ) ) ;
#5513=FACE_OUTER_BOUND ( 'NONE', #7648, .T. ) ;
#5534=CIRCLE ( 'NONE', #10757, 5.460999999999938126 ) ;
#5537=VECTOR ( 'NONE', #8048, 1000.000000000000000 ) ;
#5546=LINE ( 'NONE', #144, #13581 ) ;
#5567=FACE_OUTER_BOUND ( 'NONE', #2385, .T. ) ;
#5593=ADVANCED_FACE ( 'NONE', ( #20270 ), #18388, .F. ) ;
#5611=AXIS2_PLACEMENT_3D ( 'NONE', #2606, #9751, #7545 ) ;
#5674=DIRECTION ( 'NONE',  ( -1.159746789737949940E-14, -0.5000000000004778400, 0.8660254037841628172 ) ) ;
#5676=ORIENTED_EDGE ( 'NONE', *, *, #1557, .T. ) ;
#5684=ORIENTED_EDGE ( 'NONE', *, *, #5800, .F. ) ;
#5739=ORIENTED_EDGE ( 'NONE', *, *, #17583, .T. ) ;
#5756=DIRECTION ( 'NONE',  ( 1.000000000000000000, 4.457711412217000029E-12, 2.901972884401000201E-13 ) ) ;
#5794=ORIENTED_EDGE ( 'NONE', *, *, #8642, .F. ) ;
#5798=EDGE_LOOP ( 'NONE', ( #19616, #8244, #11886, #16263, #8019 ) ) ;
#5800=EDGE_CURVE ( 'NONE', #7394, #15975, #4377, .T. ) ;
#5829=VECTOR ( 'NONE', #19092, 1000.000000000000000 ) ;
#5856=FACE_OUTER_BOUND ( 'NONE', #6335, .T. ) ;
#5996=CARTESIAN_POINT ( 'NONE',  ( -8.890000000032001637, -3577.513800000000174, 2245.060313203000078 ) ) ;
#6013=ORIENTED_EDGE ( 'NONE', *, *, #2662, .T. ) ;
#6022=CARTESIAN_POINT ( 'NONE',  ( -6.349999999999999645, -3578.860000000000127, 2247.392000000000280 ) ) ;
#6073=DIRECTION ( 'NONE',  ( 1.000000000000000000, 0.000000000000000000, 0.000000000000000000 ) ) ;
#6080=ORIENTED_EDGE ( 'NONE', *, *, #11144, .F. ) ;
#6131=CARTESIAN_POINT ( 'NONE',  ( -12.54218463273320339, -3577.513799999517232, 2245.060313203004171 ) ) ;
#6160=DIRECTION ( 'NONE',  ( -2.318894227180156550E-14, -1.000000000000000000, 0.000000000000000000 ) ) ;
#6227=( BOUNDED_CURVE ( )  B_SPLINE_CURVE ( 3, ( #6387, #20658, #11193, #11995 ),
 .UNSPECIFIED., .F., .F. ) 
 B_SPLINE_CURVE_WITH_KNOTS ( ( 4, 4 ),
 ( 4.620504083482610562E-16, 1.570796326139804799 ),
 .UNSPECIFIED. ) 
 CURVE ( )  GEOMETRIC_REPRESENTATION_ITEM ( )  RATIONAL_B_SPLINE_CURVE ( ( 1.000000000000000000, 0.8047378542787717581, 0.8047378542787717581, 1.000000000000000000 ) ) 
 REPRESENTATION_ITEM ( '' )  );
#6279=VERTEX_POINT ( 'NONE', #1115 ) ;
#6301=EDGE_CURVE ( 'NONE', #19144, #1715, #14139, .T. ) ;
#6335=EDGE_LOOP ( 'NONE', ( #11595, #7951, #4611, #2206 ) ) ;
#6343=DIRECTION ( 'NONE',  ( 2.339144844575037611E-14, 0.000000000000000000, 1.000000000000000000 ) ) ;
#6350=ADVANCED_FACE ( 'NONE', ( #19290, #10494 ), #17636, .F. ) ;
#6387=CARTESIAN_POINT ( 'NONE',  ( -12.31900000000003459, -3581.552400000169200, 2247.392000000001190 ) ) ;
#6445=FACE_OUTER_BOUND ( 'NONE', #758, .T. ) ;
#6452=PRODUCT_DEFINITION_CONTEXT ( 'detailed design', #8873, 'design' ) ;
#6533=LINE ( 'NONE', #13433, #5537 ) ;
#6566=DIRECTION ( 'NONE',  ( -1.000000000000000000, 2.330758767201999921E-14, 2.343004830739999973E-14 ) ) ;
#6584=DIRECTION ( 'NONE',  ( 2.330758767201999921E-14, 1.000000000000000000, -5.460979050843892707E-28 ) ) ;
#6625=CIRCLE ( 'NONE', #19722, 1.904999999999823501 ) ;
#6761=CARTESIAN_POINT ( 'NONE',  ( -6.349999999999999645, -3578.860000000000127, 2247.392000000000280 ) ) ;
#6794=FACE_OUTER_BOUND ( 'NONE', #19712, .T. ) ;
#6795=EDGE_LOOP ( 'NONE', ( #15260, #1146, #13820, #15284 ) ) ;
#6801=ORIENTED_EDGE ( 'NONE', *, *, #19432, .F. ) ;
#6812=DIRECTION ( 'NONE',  ( -1.000000000000000000, 0.000000000000000000, 0.000000000000000000 ) ) ;
#6820=CARTESIAN_POINT ( 'NONE',  ( -12.69999999979383887, -3575.985370510264602, 2247.391999999993459 ) ) ;
#6881=EDGE_CURVE ( 'NONE', #2597, #15615, #7388, .T. ) ;
#6906=ORIENTED_EDGE ( 'NONE', *, *, #8942, .T. ) ;
#6908=CARTESIAN_POINT ( 'NONE',  ( -6.730999999999880856, -3578.860000000000127, 2252.472000000000207 ) ) ;
#6932=CARTESIAN_POINT ( 'NONE',  ( -12.31900000000012874, -3578.860000000000127, 2241.931000000000040 ) ) ;
#6935=EDGE_CURVE ( 'NONE', #12473, #12697, #12174, .T. ) ;
#6966=EDGE_CURVE ( 'NONE', #1715, #12697, #4813, .T. ) ;
#7006=VECTOR ( 'NONE', #4304, 1000.000000000000000 ) ;
#7080=EDGE_LOOP ( 'NONE', ( #7847, #9604, #20855, #21388 ) ) ;
#7084=LINE ( 'NONE', #1915, #19277 ) ;
#7115=DIRECTION ( 'NONE',  ( 1.000000000000000000, 0.000000000000000000, 0.000000000000000000 ) ) ;
#7123=DIRECTION ( 'NONE',  ( 0.000000000000000000, -1.000000000000000000, -2.848874176402999842E-12 ) ) ;
#7137=DIRECTION ( 'NONE',  ( -2.343004830739999973E-14, -1.784212334590129905E-30, -1.000000000000000000 ) ) ;
#7175=CARTESIAN_POINT ( 'NONE',  ( -6.349999999999999645, -3578.860000000000127, 2247.392000000000280 ) ) ;
#7230=VECTOR ( 'NONE', #8152, 1000.000000000000114 ) ;
#7253=EDGE_LOOP ( 'NONE', ( #13675, #19005, #9205, #21534 ) ) ;
#7271=CARTESIAN_POINT ( 'NONE',  ( -6.349999999999999645, -3584.320999999999913, 2247.392000000000280 ) ) ;
#7287=ORIENTED_EDGE ( 'NONE', *, *, #12957, .T. ) ;
#7307=AXIS2_PLACEMENT_3D ( 'NONE', #2572, #6566, #17205 ) ;
#7319=ORIENTED_EDGE ( 'NONE', *, *, #351, .T. ) ;
#7337=LINE ( 'NONE', #5348, #1298 ) ;
#7388=( BOUNDED_CURVE ( )  B_SPLINE_CURVE ( 3, ( #9740, #2822, #2493, #13610 ),
 .UNSPECIFIED., .F., .F. ) 
 B_SPLINE_CURVE_WITH_KNOTS ( ( 4, 4 ),
 ( -8.881784197001252323E-16, 1.570796326722519565 ),
 .UNSPECIFIED. ) 
 CURVE ( )  GEOMETRIC_REPRESENTATION_ITEM ( )  RATIONAL_B_SPLINE_CURVE ( ( 1.000000000000000000, 0.8047378541414241804, 0.8047378541414241804, 1.000000000000000000 ) ) 
 REPRESENTATION_ITEM ( '' )  );
#7394=VERTEX_POINT ( 'NONE', #13754 ) ;
#7410=CARTESIAN_POINT ( 'NONE',  ( -12.69999999999999929, -3578.860000000000127, 2247.392000000000280 ) ) ;
#7444=DIRECTION ( 'NONE',  ( 0.000000000000000000, 0.5000000000031962211, -0.8660254037825932949 ) ) ;
#7464=ORIENTED_EDGE ( 'NONE', *, *, #12866, .T. ) ;
#7477=FACE_OUTER_BOUND ( 'NONE', #22003, .T. ) ;
#7533=ORIENTED_EDGE ( 'NONE', *, *, #5800, .T. ) ;
#7537=CARTESIAN_POINT ( 'NONE',  ( -8.890000000024000926, -3576.167599999999766, 2247.392000000000280 ) ) ;
#7545=DIRECTION ( 'NONE',  ( 1.000000000000000000, 0.000000000000000000, 0.000000000000000000 ) ) ;
#7581=DIRECTION ( 'NONE',  ( 1.000000000000000000, 0.000000000000000000, 0.000000000000000000 ) ) ;
#7589=DIRECTION ( 'NONE',  ( -3.194481088215918719E-14, -0.5000000000040877302, -0.8660254037820785955 ) ) ;
#7645=AXIS2_PLACEMENT_3D ( 'NONE', #13174, #4276, #20218 ) ;
#7648=EDGE_LOOP ( 'NONE', ( #16356, #8002, #14497, #13722 ) ) ;
#7664=APPLICATION_CONTEXT ( 'configuration controlled 3d designs of mechanical parts and assemblies' ) ;
#7721=EDGE_CURVE ( 'NONE', #2758, #8066, #3764, .T. ) ;
#7762=CARTESIAN_POINT ( 'NONE',  ( -12.54218463262943217, -3580.206200000482568, 2245.060313202995985 ) ) ;
#7840=DIRECTION ( 'NONE',  ( 0.000000000000000000, 0.8660254037838039931, 0.5000000000010993428 ) ) ;
#7846=LINE ( 'NONE', #17083, #8390 ) ;
#7847=ORIENTED_EDGE ( 'NONE', *, *, #4726, .F. ) ;
#7863=LINE ( 'NONE', #5996, #20433 ) ;
#7868=VERTEX_POINT ( 'NONE', #3824 ) ;
#7929=VERTEX_POINT ( 'NONE', #20674 ) ;
#7951=ORIENTED_EDGE ( 'NONE', *, *, #17583, .F. ) ;
#7977=CIRCLE ( 'NONE', #10227, 5.079999999999973426 ) ;
#8002=ORIENTED_EDGE ( 'NONE', *, *, #6881, .T. ) ;
#8019=ORIENTED_EDGE ( 'NONE', *, *, #10984, .F. ) ;
#8048=DIRECTION ( 'NONE',  ( 3.410944169536999938E-12, -1.000000000000000000, -9.896505939572001285E-13 ) ) ;
#8066=VERTEX_POINT ( 'NONE', #19507 ) ;
#8098=LINE ( 'NONE', #8205, #17099 ) ;
#8107=CARTESIAN_POINT ( 'NONE',  ( -12.69999999999999929, -3578.860000000000127, 2247.392000000000280 ) ) ;
#8149=CARTESIAN_POINT ( 'NONE',  ( -12.31900000000000084, -3578.860000000000127, 2247.392000000000280 ) ) ;
#8152=DIRECTION ( 'NONE',  ( -3.592637833098024570E-12, 0.5000000000004030110, -0.8660254037842058938 ) ) ;
#8205=CARTESIAN_POINT ( 'NONE',  ( -12.31900000000000084, -3577.513800000000174, 2245.060313203000078 ) ) ;
#8244=ORIENTED_EDGE ( 'NONE', *, *, #10684, .T. ) ;
#8246=CIRCLE ( 'NONE', #8620, 3.175000000000149925 ) ;
#8256=VERTEX_POINT ( 'NONE', #174 ) ;
#8273=DIRECTION ( 'NONE',  ( 0.000000000000000000, -1.000000000000000000, 0.000000000000000000 ) ) ;
#8390=VECTOR ( 'NONE', #1030, 1000.000000000000000 ) ;
#8443=AXIS2_PLACEMENT_3D ( 'NONE', #3146, #8552, #15694 ) ;
#8503=CIRCLE ( 'NONE', #1383, 5.079999999999973426 ) ;
#8513=ADVANCED_BREP_SHAPE_REPRESENTATION ( '', ( #13479, #5611 ), #12354 ) ;
#8517=TOROIDAL_SURFACE ( 'NONE', #17115, 5.080000000000000071, 0.3810000000000000053 ) ;
#8533=VERTEX_POINT ( 'NONE', #10576 ) ;
#8552=DIRECTION ( 'NONE',  ( 3.194481088216070180E-14, 0.5000000000047110094, 0.8660254037817188832 ) ) ;
#8615=SHAPE_REPRESENTATION ( 'Screw 1', ( #5611 ), #12354 ) ;
#8620=AXIS2_PLACEMENT_3D ( 'NONE', #11321, #7581, #11107 ) ;
#8642=EDGE_CURVE ( 'NONE', #15975, #7394, #6625, .T. ) ;
#8674=ORIENTED_EDGE ( 'NONE', *, *, #14428, .T. ) ;
#8745=AXIS2_PLACEMENT_3D ( 'NONE', #4901, #20598, #20491 ) ;
#8748=CARTESIAN_POINT ( 'NONE',  ( -6.730999999999872863, -3578.860000000000127, 2252.853000000000065 ) ) ;
#8776=EDGE_CURVE ( 'NONE', #14878, #7394, #14889, .T. ) ;
#8800=CARTESIAN_POINT ( 'NONE',  ( -12.31900000000000084, -3580.206200000000081, 2245.060313203000078 ) ) ;
#8821=FACE_OUTER_BOUND ( 'NONE', #5798, .T. ) ;
#8854=ORIENTED_EDGE ( 'NONE', *, *, #2856, .F. ) ;
#8858=FACE_OUTER_BOUND ( 'NONE', #7253, .T. ) ;
#8873=APPLICATION_CONTEXT ( 'configuration controlled 3d designs of mechanical parts and assemblies' ) ;
#8899=CIRCLE ( 'NONE', #15257, 5.079999999999973426 ) ;
#8915=VERTEX_POINT ( 'NONE', #715 ) ;
#8918=EDGE_LOOP ( 'NONE', ( #21242, #20037 ) ) ;
#8931=SHAPE_REPRESENTATION_RELATIONSHIP ( 'NONE' , 'NONE' ,  #8615, #8513 ) ;
#8942=EDGE_CURVE ( 'NONE', #5409, #19963, #17456, .T. ) ;
#8947=ORIENTED_EDGE ( 'NONE', *, *, #22587, .T. ) ;
#9093=DIRECTION ( 'NONE',  ( -1.000000000000000000, 0.000000000000000000, 0.000000000000000000 ) ) ;
#9153=ADVANCED_FACE ( 'NONE', ( #13110 ), #18382, .T. ) ;
#9205=ORIENTED_EDGE ( 'NONE', *, *, #8942, .F. ) ;
#9246=DIRECTION ( 'NONE',  ( 0.000000000000000000, 1.000000000000000000, 0.000000000000000000 ) ) ;
#9348=CARTESIAN_POINT ( 'NONE',  ( -12.31900000000000084, -3578.860000000000127, 2247.392000000000280 ) ) ;
#9423=AXIS2_PLACEMENT_3D ( 'NONE', #6022, #18655, #840 ) ;
#9439=PLANE ( 'NONE',  #7645 ) ;
#9460=EDGE_LOOP ( 'NONE', ( #4073, #7287, #13384, #14860, #2828 ) ) ;
#9470=CARTESIAN_POINT ( 'NONE',  ( 19.05000000000000071, -3578.860000000000127, 2247.392000000000280 ) ) ;
#9479=CIRCLE ( 'NONE', #5375, 3.175000000000149925 ) ;
#9504=ORIENTED_EDGE ( 'NONE', *, *, #6935, .F. ) ;
#9585=CARTESIAN_POINT ( 'NONE',  ( -8.890000000022000748, -3580.206200000000081, 2245.060313203000078 ) ) ;
#9604=ORIENTED_EDGE ( 'NONE', *, *, #16409, .F. ) ;
#9605=CARTESIAN_POINT ( 'NONE',  ( -12.31900000000011985, -3578.860000000000127, 2242.311999999999898 ) ) ;
#9646=ADVANCED_FACE ( 'NONE', ( #17361 ), #11986, .T. ) ;
#9689=CARTESIAN_POINT ( 'NONE',  ( -8.890000000022000748, -3580.206200000000081, 2245.060313203000078 ) ) ;
#9733=DIRECTION ( 'NONE',  ( -1.000000000000000000, 0.000000000000000000, 0.000000000000000000 ) ) ;
#9740=CARTESIAN_POINT ( 'NONE',  ( -12.31900000000000084, -3580.206200000121044, 2249.723686796789480 ) ) ;
#9751=DIRECTION ( 'NONE',  ( 0.000000000000000000, 0.000000000000000000, 1.000000000000000000 ) ) ;
#9762=EDGE_LOOP ( 'NONE', ( #15700, #16777, #11587, #9504 ) ) ;
#9771=ORIENTED_EDGE ( 'NONE', *, *, #15101, .T. ) ;
#9848=CIRCLE ( 'NONE', #8745, 5.460999999999938126 ) ;
#9854=AXIS2_PLACEMENT_3D ( 'NONE', #7410, #14562, #2365 ) ;
#9951=AXIS2_PLACEMENT_3D ( 'NONE', #6761, #70, #16006 ) ;
#9953=DIRECTION ( 'NONE',  ( 3.414809992136075319E-14, 0.5000000000047110094, 0.8660254037817188832 ) ) ;
#9963=DIRECTION ( 'NONE',  ( 1.000000000000000000, -2.334777064353000131E-14, -2.343004830739999973E-14 ) ) ;
#9979=FACE_OUTER_BOUND ( 'NONE', #16180, .T. ) ;
#9998=ORIENTED_EDGE ( 'NONE', *, *, #20753, .T. ) ;
#10027=DIRECTION ( 'NONE',  ( -1.000000000000000000, 0.000000000000000000, 0.000000000000000000 ) ) ;
#10069=DIRECTION ( 'NONE',  ( -1.000000000000000000, 0.000000000000000000, 0.000000000000000000 ) ) ;
#10123=CARTESIAN_POINT ( 'NONE',  ( 19.05000000000000071, -3582.035000000000309, 2247.392000000000280 ) ) ;
#10227=AXIS2_PLACEMENT_3D ( 'NONE', #20643, #15043, #11739 ) ;
#10256=VECTOR ( 'NONE', #863, 999.9999999999998863 ) ;
#10411=CARTESIAN_POINT ( 'NONE',  ( -6.730999999999999872, -3578.860000000000127, 2247.392000000000280 ) ) ;
#10449=ORIENTED_EDGE ( 'NONE', *, *, #11144, .T. ) ;
#10462=ORIENTED_EDGE ( 'NONE', *, *, #3269, .T. ) ;
#10493=EDGE_LOOP ( 'NONE', ( #9998, #5676, #17615, #3004 ) ) ;
#10494=FACE_OUTER_BOUND ( 'NONE', #1782, .T. ) ;
#10502=FACE_OUTER_BOUND ( 'NONE', #7080, .T. ) ;
#10564=DIRECTION ( 'NONE',  ( -1.000000000000000000, 0.000000000000000000, 0.000000000000000000 ) ) ;
#10576=CARTESIAN_POINT ( 'NONE',  ( -6.731000000000127770, -3584.320999999999913, 2247.392000000000280 ) ) ;
#10618=CIRCLE ( 'NONE', #11727, 1.269999999999882334 ) ;
#10637=CARTESIAN_POINT ( 'NONE',  ( -12.69999999999999929, -3578.860000000000127, 2247.392000000000280 ) ) ;
#10660=TOROIDAL_SURFACE ( 'NONE', #13656, 1.905000000000000027, 1.270000000000000018 ) ;
#10684=EDGE_CURVE ( 'NONE', #1451, #13496, #10716, .T. ) ;
#10705=ORIENTED_EDGE ( 'NONE', *, *, #11975, .F. ) ;
#10716=CIRCLE ( 'NONE', #11106, 5.460999999999938126 ) ;
#10719=LINE ( 'NONE', #5451, #13219 ) ;
#10747=CARTESIAN_POINT ( 'NONE',  ( -12.31900000000000084, -3577.513800000000174, 2249.723686796999573 ) ) ;
#10757=AXIS2_PLACEMENT_3D ( 'NONE', #13953, #9963, #17111 ) ;
#10832=DIRECTION ( 'NONE',  ( -1.744130311077015631E-12, -0.5000000000049040771, -0.8660254037816071948 ) ) ;
#10867=LINE ( 'NONE', #21654, #12062 ) ;
#10922=CARTESIAN_POINT ( 'NONE',  ( -12.31900000000000084, -3578.860000000000127, 2247.392000000000280 ) ) ;
#10928=AXIS2_PLACEMENT_3D ( 'NONE', #2052, #7444, #406 ) ;
#10942=CARTESIAN_POINT ( 'NONE',  ( -12.31900000000000084, -3578.860000000000127, 2247.392000000000280 ) ) ;
#10973=CARTESIAN_POINT ( 'NONE',  ( -6.730999999999999872, -3578.860000000000127, 2247.392000000000280 ) ) ;
#10984=EDGE_CURVE ( 'NONE', #18142, #12726, #979, .T. ) ;
#11013=CARTESIAN_POINT ( 'NONE',  ( -12.70000000000005436, -3581.992340905245783, 2247.392000000001644 ) ) ;
#11106=AXIS2_PLACEMENT_3D ( 'NONE', #10942, #292, #11179 ) ;
#11107=DIRECTION ( 'NONE',  ( 0.000000000000000000, 1.000000000000000000, 0.000000000000000000 ) ) ;
#11144=EDGE_CURVE ( 'NONE', #18508, #18837, #12939, .T. ) ;
#11179=DIRECTION ( 'NONE',  ( -2.318894227180156550E-14, -1.000000000000000000, 0.000000000000000000 ) ) ;
#11193=CARTESIAN_POINT ( 'NONE',  ( -12.69999999985380867, -3581.734629489801137, 2247.392000000001644 ) ) ;
#11222=ORIENTED_EDGE ( 'NONE', *, *, #6935, .T. ) ;
#11230=PRODUCT_DEFINITION_FORMATION_WITH_SPECIFIED_SOURCE ( 'ANY', '', #19099, .NOT_KNOWN. ) ;
#11256=CARTESIAN_POINT ( 'NONE',  ( -12.69999999999997087, -3575.727659094874525, 2247.391999999782001 ) ) ;
#11266=ADVANCED_FACE ( 'NONE', ( #7477 ), #18025, .T. ) ;
#11288=EDGE_LOOP ( 'NONE', ( #2473, #15039, #12114, #10705 ) ) ;
#11321=CARTESIAN_POINT ( 'NONE',  ( 19.05000000000000071, -3578.860000000000127, 2247.392000000000280 ) ) ;
#11342=UNCERTAINTY_MEASURE_WITH_UNIT (LENGTH_MEASURE( 1.000000000000000082E-05 ), #3304, 'distance_accuracy_value', 'NONE');
#11365=ORIENTED_EDGE ( 'NONE', *, *, #15101, .F. ) ;
#11434=CARTESIAN_POINT ( 'NONE',  ( -12.31900000000000084, -3580.206200000000081, 2249.723686796999573 ) ) ;
#11470=DIRECTION ( 'NONE',  ( 2.330758767201999921E-14, 1.000000000000000000, -5.460979050843892707E-28 ) ) ;
#11511=CARTESIAN_POINT ( 'NONE',  ( -6.349999999999999645, -3578.860000000000127, 2247.392000000000280 ) ) ;
#11532=DIRECTION ( 'NONE',  ( -1.000000000000000000, 2.318894227180000040E-14, 2.343004830739999973E-14 ) ) ;
#11587=ORIENTED_EDGE ( 'NONE', *, *, #6966, .T. ) ;
#11595=ORIENTED_EDGE ( 'NONE', *, *, #2260, .F. ) ;
#11665=CIRCLE ( 'NONE', #9854, 5.079999999999973426 ) ;
#11676=ADVANCED_FACE ( 'NONE', ( #13519 ), #9439, .T. ) ;
#11698=CARTESIAN_POINT ( 'NONE',  ( -12.31900000000000084, -3580.206200000000081, 2245.060313203000078 ) ) ;
#11704=CARTESIAN_POINT ( 'NONE',  ( -12.31900000000001505, -3577.513799999857383, 2249.723686796824950 ) ) ;
#11713=EDGE_CURVE ( 'NONE', #19144, #5409, #6227, .T. ) ;
#11720=EDGE_CURVE ( 'NONE', #13851, #6279, #22411, .T. ) ;
#11727=AXIS2_PLACEMENT_3D ( 'NONE', #16184, #19709, #19822 ) ;
#11739=DIRECTION ( 'NONE',  ( 2.339144844575037611E-14, 0.000000000000000000, 1.000000000000000000 ) ) ;
#11886=ORIENTED_EDGE ( 'NONE', *, *, #22008, .T. ) ;
#11889=CARTESIAN_POINT ( 'NONE',  ( -12.31900000000000084, -3578.860000000000127, 2247.392000000000280 ) ) ;
#11934=PLANE ( 'NONE',  #887 ) ;
#11961=ADVANCED_FACE ( 'NONE', ( #15118 ), #4307, .T. ) ;
#11965=CARTESIAN_POINT ( 'NONE',  ( 19.05000000000000071, -3582.035000000000309, 2247.392000000000280 ) ) ;
#11975=EDGE_CURVE ( 'NONE', #1715, #21296, #13231, .T. ) ;
#11986=CYLINDRICAL_SURFACE ( 'NONE', #21643, 3.175000000000149925 ) ;
#11995=CARTESIAN_POINT ( 'NONE',  ( -12.70000000000005436, -3581.992340905245783, 2247.392000000001644 ) ) ;
#12050=CARTESIAN_POINT ( 'NONE',  ( -6.349999999999880629, -3578.860000000000127, 2252.472000000000207 ) ) ;
#12055=FACE_OUTER_BOUND ( 'NONE', #77, .T. ) ;
#12062=VECTOR ( 'NONE', #18016, 1000.000000000000000 ) ;
#12114=ORIENTED_EDGE ( 'NONE', *, *, #3269, .F. ) ;
#12136=ORIENTED_EDGE ( 'NONE', *, *, #14019, .T. ) ;
#12172=DIRECTION ( 'NONE',  ( 2.330758767201999921E-14, 1.000000000000000000, 0.000000000000000000 ) ) ;
#12174=( BOUNDED_CURVE ( )  B_SPLINE_CURVE ( 3, ( #18758, #22156, #6131, #13256 ),
 .UNSPECIFIED., .F., .T. ) 
 B_SPLINE_CURVE_WITH_KNOTS ( ( 4, 4 ),
 ( 1.570796326809868804, 3.141592653589801110 ),
 .UNSPECIFIED. ) 
 CURVE ( )  GEOMETRIC_REPRESENTATION_ITEM ( )  RATIONAL_B_SPLINE_CURVE ( ( 1.000000000000000000, 0.8047378541278922270, 0.8047378541278922270, 1.000000000000000000 ) ) 
 REPRESENTATION_ITEM ( '' )  );
#12182=AXIS2_PLACEMENT_3D ( 'NONE', #13463, #3030, #1267 ) ;
#12270=DIRECTION ( 'NONE',  ( -2.334777064352623371E-14, -1.000000000000000000, 0.000000000000000000 ) ) ;
#12292=FACE_OUTER_BOUND ( 'NONE', #18265, .T. ) ;
#12322=VECTOR ( 'NONE', #199, 1000.000000000000000 ) ;
#12354=( GEOMETRIC_REPRESENTATION_CONTEXT ( 3 ) GLOBAL_UNCERTAINTY_ASSIGNED_CONTEXT ( ( #11342 ) ) GLOBAL_UNIT_ASSIGNED_CONTEXT ( ( #3304, #1659, #27 ) ) REPRESENTATION_CONTEXT ( 'NONE', 'WORKASPACE' ) );
#12365=PRODUCT_DEFINITION ( 'UNKNOWN', '', #11230, #6452 ) ;
#12373=ADVANCED_FACE ( 'NONE', ( #14867 ), #10660, .T. ) ;
#12404=CYLINDRICAL_SURFACE ( 'NONE', #19991, 0.3809999999999647002 ) ;
#12473=VERTEX_POINT ( 'NONE', #4644 ) ;
#12524=AXIS2_PLACEMENT_3D ( 'NONE', #4767, #22109, #4311 ) ;
#12562=EDGE_CURVE ( 'NONE', #14878, #22087, #16990, .T. ) ;
#12572=TOROIDAL_SURFACE ( 'NONE', #20076, 1.905000000000000027, 1.270000000000000018 ) ;
#12690=ORIENTED_EDGE ( 'NONE', *, *, #16662, .F. ) ;
#12695=EDGE_CURVE ( 'NONE', #18837, #8533, #14388, .T. ) ;
#12697=VERTEX_POINT ( 'NONE', #5006 ) ;
#12726=VERTEX_POINT ( 'NONE', #15551 ) ;
#12758=ORIENTED_EDGE ( 'NONE', *, *, #17525, .T. ) ;
#12866=EDGE_CURVE ( 'NONE', #15615, #5409, #12960, .T. ) ;
#12888=CARTESIAN_POINT ( 'NONE',  ( -8.890000000028999594, -3574.821399999999812, 2245.060313203000078 ) ) ;
#12896=EDGE_LOOP ( 'NONE', ( #17580, #14695, #20874, #17549 ) ) ;
#12939=CIRCLE ( 'NONE', #5476, 0.3810000000000002829 ) ;
#12949=CIRCLE ( 'NONE', #2838, 0.3809999999999993947 ) ;
#12957=EDGE_CURVE ( 'NONE', #13496, #7929, #15508, .T. ) ;
#12960=LINE ( 'NONE', #16129, #20011 ) ;
#12987=CARTESIAN_POINT ( 'NONE',  ( -12.31900000000000084, -3581.209255678999853, 2248.748343399000532 ) ) ;
#12993=EDGE_CURVE ( 'NONE', #13145, #8256, #2740, .T. ) ;
#13110=FACE_OUTER_BOUND ( 'NONE', #10493, .T. ) ;
#13136=DIRECTION ( 'NONE',  ( 0.000000000000000000, 0.000000000000000000, -1.000000000000000000 ) ) ;
#13145=VERTEX_POINT ( 'NONE', #4739 ) ;
#13174=CARTESIAN_POINT ( 'NONE',  ( -8.890000000047999507, -3577.513800000000174, 2245.060313203000078 ) ) ;
#13193=DIRECTION ( 'NONE',  ( -3.479240369245040749E-14, -0.5000000000042060799, -0.8660254037820102058 ) ) ;
#13200=LINE ( 'NONE', #9689, #7006 ) ;
#13204=DIRECTION ( 'NONE',  ( 0.000000000000000000, 1.000000000000000000, 0.000000000000000000 ) ) ;
#13219=VECTOR ( 'NONE', #10832, 1000.000000000000114 ) ;
#13231=LINE ( 'NONE', #11698, #5829 ) ;
#13249=AXIS2_PLACEMENT_3D ( 'NONE', #5128, #14262, #12270 ) ;
#13256=CARTESIAN_POINT ( 'NONE',  ( -12.31900000000000084, -3577.513799999878302, 2245.060313203211081 ) ) ;
#13330=DIRECTION ( 'NONE',  ( 0.000000000000000000, -1.000000000000000000, 0.000000000000000000 ) ) ;
#13367=ORIENTED_EDGE ( 'NONE', *, *, #20753, .F. ) ;
#13384=ORIENTED_EDGE ( 'NONE', *, *, #4655, .T. ) ;
#13433=CARTESIAN_POINT ( 'NONE',  ( -8.890000000017000303, -3577.513800000000174, 2249.723686796999573 ) ) ;
#13446=AXIS2_PLACEMENT_3D ( 'NONE', #17281, #10027, #8273 ) ;
#13463=CARTESIAN_POINT ( 'NONE',  ( 20.32000000000000028, -3578.860000000000127, 2247.392000000000280 ) ) ;
#13479=MANIFOLD_SOLID_BREP ( 'TORNILLO5[1]', #5003 ) ;
#13496=VERTEX_POINT ( 'NONE', #20198 ) ;
#13519=FACE_OUTER_BOUND ( 'NONE', #16388, .T. ) ;
#13559=VECTOR ( 'NONE', #21531, 1000.000000000000000 ) ;
#13581=VECTOR ( 'NONE', #4002, 999.9999999999998863 ) ;
#13604=ADVANCED_FACE ( 'NONE', ( #9979 ), #22256, .T. ) ;
#13610=CARTESIAN_POINT ( 'NONE',  ( -12.69999999999999929, -3580.426170453010855, 2250.104686796980332 ) ) ;
#13612=ORIENTED_EDGE ( 'NONE', *, *, #22679, .F. ) ;
#13656=AXIS2_PLACEMENT_3D ( 'NONE', #9470, #563, #9246 ) ;
#13661=FACE_OUTER_BOUND ( 'NONE', #3777, .T. ) ;
#13669=TOROIDAL_SURFACE ( 'NONE', #17401, 5.080000000000000071, 0.3810000000000000053 ) ;
#13675=ORIENTED_EDGE ( 'NONE', *, *, #6301, .T. ) ;
#13722=ORIENTED_EDGE ( 'NONE', *, *, #1557, .F. ) ;
#13754=CARTESIAN_POINT ( 'NONE',  ( 20.32000000000000028, -3576.955000000000382, 2247.392000000000280 ) ) ;
#13802=ORIENTED_EDGE ( 'NONE', *, *, #2823, .F. ) ;
#13820=ORIENTED_EDGE ( 'NONE', *, *, #14557, .F. ) ;
#13851=VERTEX_POINT ( 'NONE', #11256 ) ;
#13953=CARTESIAN_POINT ( 'NONE',  ( -6.730999999999999872, -3578.860000000000127, 2247.392000000000280 ) ) ;
#14019=EDGE_CURVE ( 'NONE', #7868, #19336, #15295, .T. ) ;
#14053=DIRECTION ( 'NONE',  ( -2.330758767202000237E-14, -1.000000000000000000, -1.224646799141892318E-16 ) ) ;
#14074=DIRECTION ( 'NONE',  ( -1.000000000000000000, -1.295098308114000000E-13, 0.000000000000000000 ) ) ;
#14139=LINE ( 'NONE', #16121, #22289 ) ;
#14150=CARTESIAN_POINT ( 'NONE',  ( -8.890000000006001102, -3580.206200000000081, 2249.723686796999573 ) ) ;
#14212=SHAPE_DEFINITION_REPRESENTATION ( #16126, #8615 ) ;
#14262=DIRECTION ( 'NONE',  ( 1.000000000000000000, -2.334777064353000131E-14, -2.343004830739999973E-14 ) ) ;
#14266=CARTESIAN_POINT ( 'NONE',  ( -8.890000000026999416, -3576.167599999999766, 2247.392000000000280 ) ) ;
#14277=AXIS2_PLACEMENT_3D ( 'NONE', #11889, #11532, #2627 ) ;
#14283=DIRECTION ( 'NONE',  ( 0.000000000000000000, 2.331176954593720496E-12, -1.000000000000000000 ) ) ;
#14299=ORIENTED_EDGE ( 'NONE', *, *, #22587, .F. ) ;
#14328=CARTESIAN_POINT ( 'NONE',  ( -6.349999999999999645, -3575.684999999999945, 2247.392000000000280 ) ) ;
#14388=CIRCLE ( 'NONE', #13249, 5.460999999999938126 ) ;
#14400=DIRECTION ( 'NONE',  ( 0.000000000000000000, -0.8660254037817070039, 0.5000000000047313264 ) ) ;
#14428=EDGE_CURVE ( 'NONE', #19336, #1398, #10719, .T. ) ;
#14497=ORIENTED_EDGE ( 'NONE', *, *, #1065, .T. ) ;
#14532=ORIENTED_EDGE ( 'NONE', *, *, #12562, .T. ) ;
#14533=EDGE_CURVE ( 'NONE', #18508, #21577, #7977, .T. ) ;
#14557=EDGE_CURVE ( 'NONE', #8066, #2758, #9479, .T. ) ;
#14562=DIRECTION ( 'NONE',  ( -1.000000000000000000, 2.330758767201999921E-14, 2.356218894535000080E-14 ) ) ;
#14565=DIRECTION ( 'NONE',  ( -2.343004830739999973E-14, -1.784212334590129905E-30, -1.000000000000000000 ) ) ;
#14695=ORIENTED_EDGE ( 'NONE', *, *, #4677, .F. ) ;
#14696=DIRECTION ( 'NONE',  ( 0.000000000000000000, 0.5000000000005969669, -0.8660254037840939834 ) ) ;
#14758=ORIENTED_EDGE ( 'NONE', *, *, #12993, .T. ) ;
#14838=EDGE_CURVE ( 'NONE', #12726, #17006, #11665, .T. ) ;
#14860=ORIENTED_EDGE ( 'NONE', *, *, #10984, .T. ) ;
#14867=FACE_OUTER_BOUND ( 'NONE', #17772, .T. ) ;
#14869=DIRECTION ( 'NONE',  ( 0.000000000000000000, 1.206582004152999850E-12, -1.000000000000000000 ) ) ;
#14878=VERTEX_POINT ( 'NONE', #4456 ) ;
#14889=CIRCLE ( 'NONE', #3631, 1.270000000000000240 ) ;
#14905=LINE ( 'NONE', #4346, #5109 ) ;
#14974=CARTESIAN_POINT ( 'NONE',  ( 19.05000000000000071, -3578.860000000000127, 2247.392000000000280 ) ) ;
#15039=ORIENTED_EDGE ( 'NONE', *, *, #18364, .F. ) ;
#15043=DIRECTION ( 'NONE',  ( 1.000000000000000000, -2.330758767201999921E-14, -2.339144844575000061E-14 ) ) ;
#15091=DIRECTION ( 'NONE',  ( -1.000000000000000000, 0.000000000000000000, 0.000000000000000000 ) ) ;
#15101=EDGE_CURVE ( 'NONE', #21296, #1398, #17072, .T. ) ;
#15118=FACE_OUTER_BOUND ( 'NONE', #9460, .T. ) ;
#15221=CARTESIAN_POINT ( 'NONE',  ( 20.32000000000000028, -3578.860000000000127, 2247.392000000000280 ) ) ;
#15252=DIRECTION ( 'NONE',  ( -2.356218894535439317E-14, 0.000000000000000000, -1.000000000000000000 ) ) ;
#15257=AXIS2_PLACEMENT_3D ( 'NONE', #8107, #22839, #15252 ) ;
#15260=ORIENTED_EDGE ( 'NONE', *, *, #12562, .F. ) ;
#15284=ORIENTED_EDGE ( 'NONE', *, *, #19174, .F. ) ;
#15295=LINE ( 'NONE', #4624, #7230 ) ;
#15338=ORIENTED_EDGE ( 'NONE', *, *, #10684, .F. ) ;
#15373=EDGE_LOOP ( 'NONE', ( #5204, #22165, #16128, #5794 ) ) ;
#15436=FACE_OUTER_BOUND ( 'NONE', #6795, .T. ) ;
#15454=ADVANCED_FACE ( 'NONE', ( #16027 ), #23151, .T. ) ;
#15508=CIRCLE ( 'NONE', #5421, 5.460999999999938126 ) ;
#15509=ORIENTED_EDGE ( 'NONE', *, *, #2896, .T. ) ;
#15510=CARTESIAN_POINT ( 'NONE',  ( -12.69999999999999929, -3575.727659095000035, 2247.392000000000280 ) ) ;
#15548=DIRECTION ( 'NONE',  ( -1.000000000000000000, 0.000000000000000000, 0.000000000000000000 ) ) ;
#15551=CARTESIAN_POINT ( 'NONE',  ( -12.70000000000011831, -3578.860000000000127, 2242.311999999999898 ) ) ;
#15576=FACE_BOUND ( 'NONE', #329, .T. ) ;
#15615=VERTEX_POINT ( 'NONE', #17390 ) ;
#15672=PLANE ( 'NONE',  #1330 ) ;
#15676=ORIENTED_EDGE ( 'NONE', *, *, #6881, .F. ) ;
#15686=AXIS2_PLACEMENT_3D ( 'NONE', #10973, #5484, #21753 ) ;
#15694=DIRECTION ( 'NONE',  ( 0.000000000000000000, 0.8660254037817070039, -0.5000000000047313264 ) ) ;
#15700=ORIENTED_EDGE ( 'NONE', *, *, #2856, .T. ) ;
#15736=DIRECTION ( 'NONE',  ( 1.000000000000000000, 0.000000000000000000, 0.000000000000000000 ) ) ;
#15753=AXIS2_PLACEMENT_3D ( 'NONE', #1160, #10069, #1050 ) ;
#15772=EDGE_LOOP ( 'NONE', ( #10462, #14758, #625, #12136, #8674, #11365 ) ) ;
#15829=LINE ( 'NONE', #19459, #3481 ) ;
#15963=ORIENTED_EDGE ( 'NONE', *, *, #2768, .T. ) ;
#15975=VERTEX_POINT ( 'NONE', #20098 ) ;
#16006=DIRECTION ( 'NONE',  ( 2.330758767201999921E-14, 1.000000000000000000, 0.000000000000000000 ) ) ;
#16027=FACE_OUTER_BOUND ( 'NONE', #16106, .T. ) ;
#16102=DIRECTION ( 'NONE',  ( 0.000000000000000000, -0.8660254037840939834, -0.5000000000005969669 ) ) ;
#16106=EDGE_LOOP ( 'NONE', ( #4366, #22224, #9771, #15509 ) ) ;
#16121=CARTESIAN_POINT ( 'NONE',  ( -12.31900000000000084, -3581.552400000000034, 2247.392000000000280 ) ) ;
#16126=PRODUCT_DEFINITION_SHAPE ( 'NONE', 'NONE',  #12365 ) ;
#16128=ORIENTED_EDGE ( 'NONE', *, *, #8776, .T. ) ;
#16129=CARTESIAN_POINT ( 'NONE',  ( -12.69999999999999929, -3580.426170452999941, 2250.104686796999886 ) ) ;
#16131=CARTESIAN_POINT ( 'NONE',  ( -6.350000000000118661, -3578.860000000000127, 2242.311999999999898 ) ) ;
#16180=EDGE_LOOP ( 'NONE', ( #6080, #5136, #17651, #8947, #3748 ) ) ;
#16184=CARTESIAN_POINT ( 'NONE',  ( 19.05000000000000071, -3580.764999999999873, 2247.392000000000280 ) ) ;
#16246=LINE ( 'NONE', #14266, #12322 ) ;
#16263=ORIENTED_EDGE ( 'NONE', *, *, #14838, .F. ) ;
#16300=EDGE_CURVE ( 'NONE', #19963, #1715, #20573, .T. ) ;
#16356=ORIENTED_EDGE ( 'NONE', *, *, #2260, .T. ) ;
#16388=EDGE_LOOP ( 'NONE', ( #13802, #18760, #973, #20765 ) ) ;
#16409=EDGE_CURVE ( 'NONE', #8256, #2597, #5252, .T. ) ;
#16432=ORIENTED_EDGE ( 'NONE', *, *, #14533, .T. ) ;
#16485=DIRECTION ( 'NONE',  ( -1.000000000000000000, 2.318894227180000040E-14, 2.343004830739999973E-14 ) ) ;
#16500=CYLINDRICAL_SURFACE ( 'NONE', #19415, 0.3809999999999647002 ) ;
#16662=EDGE_CURVE ( 'NONE', #4945, #7929, #10867, .T. ) ;
#16695=AXIS2_PLACEMENT_3D ( 'NONE', #9605, #11470, #16753 ) ;
#16730=CARTESIAN_POINT ( 'NONE',  ( -8.890000000018000392, -3577.513800000000174, 2249.723686796999573 ) ) ;
#16741=UNCERTAINTY_MEASURE_WITH_UNIT (LENGTH_MEASURE( 1.000000000000000082E-05 ), #21126, 'distance_accuracy_value', 'NONE');
#16753=DIRECTION ( 'NONE',  ( -1.000000000000000000, 0.000000000000000000, 0.000000000000000000 ) ) ;
#16777=ORIENTED_EDGE ( 'NONE', *, *, #16300, .T. ) ;
#16929=ADVANCED_FACE ( 'NONE', ( #8858 ), #1936, .T. ) ;
#16990=CIRCLE ( 'NONE', #12524, 3.175000000000149925 ) ;
#17006=VERTEX_POINT ( 'NONE', #18780 ) ;
#17008=DIRECTION ( 'NONE',  ( 1.163002179514000079E-14, 1.000000000000000000, 7.088775189419001325E-13 ) ) ;
#17072=LINE ( 'NONE', #2779, #19166 ) ;
#17083=CARTESIAN_POINT ( 'NONE',  ( -8.890000000008999592, -3581.552400000000034, 2247.392000000000280 ) ) ;
#17099=VECTOR ( 'NONE', #9953, 999.9999999999998863 ) ;
#17111=DIRECTION ( 'NONE',  ( -2.334777064352623371E-14, -1.000000000000000000, 0.000000000000000000 ) ) ;
#17115=AXIS2_PLACEMENT_3D ( 'NONE', #10922, #22983, #14565 ) ;
#17121=AXIS2_PLACEMENT_3D ( 'NONE', #20487, #2333, #7840 ) ;
#17123=CARTESIAN_POINT ( 'NONE',  ( -12.69999999999999929, -3580.426170452999941, 2250.104686796999886 ) ) ;
#17145=ORIENTED_EDGE ( 'NONE', *, *, #12695, .F. ) ;
#17205=DIRECTION ( 'NONE',  ( -2.343004830739999973E-14, -1.784212334590129905E-30, -1.000000000000000000 ) ) ;
#17281=CARTESIAN_POINT ( 'NONE',  ( -6.349999999999999645, -3578.860000000000127, 2247.392000000000280 ) ) ;
#17361=FACE_OUTER_BOUND ( 'NONE', #12896, .T. ) ;
#17390=CARTESIAN_POINT ( 'NONE',  ( -12.69999999999999929, -3580.426170453010855, 2250.104686796980332 ) ) ;
#17401=AXIS2_PLACEMENT_3D ( 'NONE', #10411, #3376, #7137 ) ;
#17404=DIRECTION ( 'NONE',  ( 0.000000000000000000, 0.8660254037820785955, -0.5000000000040877302 ) ) ;
#17426=ORIENTED_EDGE ( 'NONE', *, *, #17860, .F. ) ;
#17456=LINE ( 'NONE', #19105, #4386 ) ;
#17517=ORIENTED_EDGE ( 'NONE', *, *, #11713, .T. ) ;
#17525=EDGE_CURVE ( 'NONE', #8533, #1451, #22960, .T. ) ;
#17549=ORIENTED_EDGE ( 'NONE', *, *, #7721, .F. ) ;
#17580=ORIENTED_EDGE ( 'NONE', *, *, #19120, .F. ) ;
#17583=EDGE_CURVE ( 'NONE', #7868, #8915, #15829, .T. ) ;
#17615=ORIENTED_EDGE ( 'NONE', *, *, #11720, .F. ) ;
#17636=PLANE ( 'NONE',  #9951 ) ;
#17651=ORIENTED_EDGE ( 'NONE', *, *, #3973, .T. ) ;
#17669=DIRECTION ( 'NONE',  ( 1.000000000000000000, 0.000000000000000000, 0.000000000000000000 ) ) ;
#17732=ORIENTED_EDGE ( 'NONE', *, *, #3973, .F. ) ;
#17757=DIRECTION ( 'NONE',  ( -2.061772070699084901E-14, 0.5000000000031208369, -0.8660254037826368156 ) ) ;
#17772=EDGE_LOOP ( 'NONE', ( #14532, #7319, #5684, #335 ) ) ;
#17860=EDGE_CURVE ( 'NONE', #4945, #18837, #9848, .T. ) ;
#17880=CARTESIAN_POINT ( 'NONE',  ( -12.31900000000003459, -3581.552400000169200, 2247.392000000001190 ) ) ;
#17923=DIRECTION ( 'NONE',  ( -1.000000000000000000, 0.000000000000000000, 0.000000000000000000 ) ) ;
#18016=DIRECTION ( 'NONE',  ( -1.000000000000000000, 0.000000000000000000, 0.000000000000000000 ) ) ;
#18025=CYLINDRICAL_SURFACE ( 'NONE', #595, 0.3809999999999121312 ) ;
#18045=VECTOR ( 'NONE', #1606, 1000.000000000000000 ) ;
#18060=CARTESIAN_POINT ( 'NONE',  ( -6.730999999999999872, -3578.860000000000127, 2247.392000000000280 ) ) ;
#18142=VERTEX_POINT ( 'NONE', #6932 ) ;
#18224=CARTESIAN_POINT ( 'NONE',  ( -6.731000000000127770, -3578.860000000000127, 2241.931000000000040 ) ) ;
#18265=EDGE_LOOP ( 'NONE', ( #22207, #22368 ) ) ;
#18287=CARTESIAN_POINT ( 'NONE',  ( -8.890000000032001637, -3577.513800000000174, 2245.060313203000078 ) ) ;
#18364=EDGE_CURVE ( 'NONE', #13145, #19144, #7846, .T. ) ;
#18382=CYLINDRICAL_SURFACE ( 'NONE', #17121, 0.3810000000000151599 ) ;
#18388=PLANE ( 'NONE',  #3251 ) ;
#18419=ADVANCED_FACE ( 'NONE', ( #15576, #12292 ), #11934, .T. ) ;
#18423=ORIENTED_EDGE ( 'NONE', *, *, #1065, .F. ) ;
#18468=ADVANCED_FACE ( 'NONE', ( #20268 ), #12404, .T. ) ;
#18508=VERTEX_POINT ( 'NONE', #12050 ) ;
#18655=DIRECTION ( 'NONE',  ( -1.000000000000000000, 0.000000000000000000, 0.000000000000000000 ) ) ;
#18758=CARTESIAN_POINT ( 'NONE',  ( -12.69999999999999929, -3577.293829546977122, 2244.679313203000220 ) ) ;
#18760=ORIENTED_EDGE ( 'NONE', *, *, #2896, .F. ) ;
#18780=CARTESIAN_POINT ( 'NONE',  ( -12.69999999999988027, -3578.860000000000127, 2252.472000000000207 ) ) ;
#18795=CARTESIAN_POINT ( 'NONE',  ( -8.890000000008999592, -3581.552400000000034, 2247.392000000000280 ) ) ;
#18837=VERTEX_POINT ( 'NONE', #8748 ) ;
#18862=CARTESIAN_POINT ( 'NONE',  ( -12.54218463268301775, -3577.513799999511775, 2249.723686797000937 ) ) ;
#18913=AXIS2_PLACEMENT_3D ( 'NONE', #4312, #15091, #13330 ) ;
#18977=PLANE ( 'NONE',  #12182 ) ;
#19005=ORIENTED_EDGE ( 'NONE', *, *, #16300, .F. ) ;
#19084=DIRECTION ( 'NONE',  ( -1.000000000000000000, 2.330758767201999921E-14, 2.343004830739999973E-14 ) ) ;
#19092=DIRECTION ( 'NONE',  ( 1.000000000000000000, -3.885294924347999634E-13, 0.000000000000000000 ) ) ;
#19099=PRODUCT ( 'Screw 1', 'Screw 1', '', ( #2842 ) ) ;
#19105=CARTESIAN_POINT ( 'NONE',  ( -12.69999999999999929, -3581.992340905000219, 2247.392000000000280 ) ) ;
#19120=EDGE_CURVE ( 'NONE', #14878, #2758, #7337, .T. ) ;
#19139=CARTESIAN_POINT ( 'NONE',  ( 19.05000000000000071, -3578.860000000000127, 2247.392000000000280 ) ) ;
#19144=VERTEX_POINT ( 'NONE', #17880 ) ;
#19166=VECTOR ( 'NONE', #4201, 1000.000000000000000 ) ;
#19174=EDGE_CURVE ( 'NONE', #22087, #8066, #3056, .T. ) ;
#19209=CYLINDRICAL_SURFACE ( 'NONE', #8443, 0.3809999999999121312 ) ;
#19251=CARTESIAN_POINT ( 'NONE',  ( 20.32000000000000028, -3578.860000000000127, 2247.392000000000280 ) ) ;
#19277=VECTOR ( 'NONE', #5674, 999.9999999999998863 ) ;
#19290=FACE_BOUND ( 'NONE', #8918, .T. ) ;
#19315=AXIS2_PLACEMENT_3D ( 'NONE', #14150, #17404, #15548 ) ;
#19336=VERTEX_POINT ( 'NONE', #5180 ) ;
#19357=ORIENTED_EDGE ( 'NONE', *, *, #4726, .T. ) ;
#19415=AXIS2_PLACEMENT_3D ( 'NONE', #3498, #21555, #339 ) ;
#19432=EDGE_CURVE ( 'NONE', #13851, #2102, #4564, .T. ) ;
#19436=DIRECTION ( 'NONE',  ( 2.330758767208999958E-14, 1.000000000000000000, 2.848874176402999842E-12 ) ) ;
#19459=CARTESIAN_POINT ( 'NONE',  ( -8.890000000017000303, -3577.513800000000174, 2249.723686796999573 ) ) ;
#19507=CARTESIAN_POINT ( 'NONE',  ( -6.349999999999999645, -3582.035000000000309, 2247.392000000000280 ) ) ;
#19525=ORIENTED_EDGE ( 'NONE', *, *, #2823, .T. ) ;
#19616=ORIENTED_EDGE ( 'NONE', *, *, #746, .T. ) ;
#19655=DIRECTION ( 'NONE',  ( 0.000000000000000000, -2.848874176402999842E-12, 1.000000000000000000 ) ) ;
#19709=DIRECTION ( 'NONE',  ( -0.000000000000000000, 1.224646799147353207E-16, 1.000000000000000000 ) ) ;
#19712=EDGE_LOOP ( 'NONE', ( #1016, #10449, #4372, #22876, #17732 ) ) ;
#19714=DIRECTION ( 'NONE',  ( -1.000000000000000000, 2.330758767201999921E-14, 2.343004830739999973E-14 ) ) ;
#19722=AXIS2_PLACEMENT_3D ( 'NONE', #19251, #15736, #3653 ) ;
#19755=ADVANCED_FACE ( 'NONE', ( #6445 ), #18977, .F. ) ;
#19822=DIRECTION ( 'NONE',  ( 0.000000000000000000, -1.000000000000000000, 0.000000000000000000 ) ) ;
#19860=ADVANCED_FACE ( 'NONE', ( #6794 ), #13669, .T. ) ;
#19915=ORIENTED_EDGE ( 'NONE', *, *, #17525, .F. ) ;
#19963=VERTEX_POINT ( 'NONE', #5154 ) ;
#19968=ORIENTED_EDGE ( 'NONE', *, *, #4655, .F. ) ;
#19978=ADVANCED_FACE ( 'NONE', ( #12055 ), #19209, .T. ) ;
#19991=AXIS2_PLACEMENT_3D ( 'NONE', #22931, #19436, #14283 ) ;
#20011=VECTOR ( 'NONE', #5356, 1000.000000000000000 ) ;
#20037=ORIENTED_EDGE ( 'NONE', *, *, #7721, .T. ) ;
#20076=AXIS2_PLACEMENT_3D ( 'NONE', #14974, #6073, #13204 ) ;
#20098=CARTESIAN_POINT ( 'NONE',  ( 20.32000000000000028, -3580.764999999999873, 2247.392000000000280 ) ) ;
#20187=ADVANCED_FACE ( 'NONE', ( #22105 ), #12572, .T. ) ;
#20198=CARTESIAN_POINT ( 'NONE',  ( -12.31899999999987116, -3578.860000000000127, 2252.853000000000065 ) ) ;
#20218=DIRECTION ( 'NONE',  ( -1.000000000000000000, 0.000000000000000000, 0.000000000000000000 ) ) ;
#20268=FACE_OUTER_BOUND ( 'NONE', #9762, .T. ) ;
#20270=FACE_OUTER_BOUND ( 'NONE', #15772, .T. ) ;
#20327=ADVANCED_FACE ( 'NONE', ( #10502 ), #3118, .T. ) ;
#20396=AXIS2_PLACEMENT_3D ( 'NONE', #18060, #19714, #263 ) ;
#20433=VECTOR ( 'NONE', #20735, 1000.000000000000000 ) ;
#20487=CARTESIAN_POINT ( 'NONE',  ( -12.31900000000000084, -3576.510744320999947, 2248.748343399000532 ) ) ;
#20491=DIRECTION ( 'NONE',  ( -2.334777064352623371E-14, -1.000000000000000000, 0.000000000000000000 ) ) ;
#20564=CARTESIAN_POINT ( 'NONE',  ( -6.730999999999872863, -3573.399000000000342, 2247.392000000000280 ) ) ;
#20573=( BOUNDED_CURVE ( )  B_SPLINE_CURVE ( 3, ( #2370, #20713, #7762, #4013 ),
 .UNSPECIFIED., .F., .T. ) 
 B_SPLINE_CURVE_WITH_KNOTS ( ( 4, 4 ),
 ( 1.570796327396364100, 3.141592653589738937 ),
 .UNSPECIFIED. ) 
 CURVE ( )  GEOMETRIC_REPRESENTATION_ITEM ( )  RATIONAL_B_SPLINE_CURVE ( ( 1.000000000000000000, 0.8047378542661449696, 0.8047378542661449696, 1.000000000000000000 ) ) 
 REPRESENTATION_ITEM ( '' )  );
#20598=DIRECTION ( 'NONE',  ( 1.000000000000000000, -2.334777064353000131E-14, -2.343004830739999973E-14 ) ) ;
#20636=LINE ( 'NONE', #17123, #4537 ) ;
#20643=CARTESIAN_POINT ( 'NONE',  ( -6.349999999999999645, -3578.860000000000127, 2247.392000000000280 ) ) ;
#20658=CARTESIAN_POINT ( 'NONE',  ( -12.54218463261993577, -3581.552400000410671, 2247.392000000001190 ) ) ;
#20674=CARTESIAN_POINT ( 'NONE',  ( -12.31899999999987294, -3573.399000000000342, 2247.392000000000280 ) ) ;
#20685=VECTOR ( 'NONE', #17923, 1000.000000000000000 ) ;
#20713=CARTESIAN_POINT ( 'NONE',  ( -12.69999999986577244, -3580.297314745182575, 2244.902497835854319 ) ) ;
#20735=DIRECTION ( 'NONE',  ( -1.000000000000000000, -2.590196616239000129E-13, 3.885294924357999613E-13 ) ) ;
#20753=EDGE_CURVE ( 'NONE', #2102, #8915, #7084, .T. ) ;
#20765=ORIENTED_EDGE ( 'NONE', *, *, #22679, .T. ) ;
#20855=ORIENTED_EDGE ( 'NONE', *, *, #12993, .F. ) ;
#20856=AXIS2_PLACEMENT_3D ( 'NONE', #4809, #6584, #6812 ) ;
#20874=ORIENTED_EDGE ( 'NONE', *, *, #19174, .T. ) ;
#20954=CARTESIAN_POINT ( 'NONE',  ( -8.890000000008001280, -3580.206200000000081, 2249.723686796999573 ) ) ;
#20957=DIRECTION ( 'NONE',  ( 1.000000000000000000, 0.000000000000000000, 0.000000000000000000 ) ) ;
#21126=( LENGTH_UNIT ( ) NAMED_UNIT ( * ) SI_UNIT ( .MILLI., .METRE. ) );
#21242=ORIENTED_EDGE ( 'NONE', *, *, #14557, .T. ) ;
#21249=ADVANCED_FACE ( 'NONE', ( #5856 ), #5295, .T. ) ;
#21296=VERTEX_POINT ( 'NONE', #9585 ) ;
#21325=ORIENTED_EDGE ( 'NONE', *, *, #746, .F. ) ;
#21388=ORIENTED_EDGE ( 'NONE', *, *, #18364, .T. ) ;
#21420=ADVANCED_FACE ( 'NONE', ( #15436 ), #1011, .T. ) ;
#21466=ADVANCED_FACE ( 'NONE', ( #4531 ), #15672, .T. ) ;
#21475=CARTESIAN_POINT ( 'NONE',  ( 19.05000000000000071, -3576.955000000000382, 2247.392000000000280 ) ) ;
#21531=DIRECTION ( 'NONE',  ( -1.417468298637000021E-14, -1.000000000000000000, -1.319534125277000180E-12 ) ) ;
#21534=ORIENTED_EDGE ( 'NONE', *, *, #11713, .F. ) ;
#21536=CARTESIAN_POINT ( 'NONE',  ( -8.890000000036000216, -3580.206200000000081, 2245.060313203000078 ) ) ;
#21555=DIRECTION ( 'NONE',  ( -2.330758767204999802E-14, -1.000000000000000000, -1.206582004152999850E-12 ) ) ;
#21577=VERTEX_POINT ( 'NONE', #16131 ) ;
#21643=AXIS2_PLACEMENT_3D ( 'NONE', #19139, #3076, #1553 ) ;
#21654=CARTESIAN_POINT ( 'NONE',  ( -6.349999999999999645, -3573.399000000000342, 2247.392000000000280 ) ) ;
#21747=AXIS2_PLACEMENT_3D ( 'NONE', #7537, #16102, #14696 ) ;
#21753=DIRECTION ( 'NONE',  ( -2.334777064352623371E-14, -1.000000000000000000, 0.000000000000000000 ) ) ;
#21794=DIRECTION ( 'NONE',  ( -4.457711412217000029E-12, 1.000000000000000000, 0.000000000000000000 ) ) ;
#21989=DIRECTION ( 'NONE',  ( -2.318894227180156550E-14, -1.000000000000000000, 0.000000000000000000 ) ) ;
#22003=EDGE_LOOP ( 'NONE', ( #19357, #17517, #2266, #15676 ) ) ;
#22008=EDGE_CURVE ( 'NONE', #13496, #17006, #12949, .T. ) ;
#22023=ORIENTED_EDGE ( 'NONE', *, *, #11720, .T. ) ;
#22052=CYLINDRICAL_SURFACE ( 'NONE', #9423, 5.460999999999938126 ) ;
#22080=DIRECTION ( 'NONE',  ( -1.000000000000000000, 2.318894227180000040E-14, 2.343004830739999973E-14 ) ) ;
#22087=VERTEX_POINT ( 'NONE', #10123 ) ;
#22105=FACE_OUTER_BOUND ( 'NONE', #15373, .T. ) ;
#22109=DIRECTION ( 'NONE',  ( 1.000000000000000000, 0.000000000000000000, 0.000000000000000000 ) ) ;
#22119=CIRCLE ( 'NONE', #14277, 5.460999999999938126 ) ;
#22156=CARTESIAN_POINT ( 'NONE',  ( -12.69999999999666507, -3577.422685254746739, 2244.902497835742906 ) ) ;
#22165=ORIENTED_EDGE ( 'NONE', *, *, #4677, .T. ) ;
#22176=ADVANCED_FACE ( 'NONE', ( #5513 ), #16500, .T. ) ;
#22207=ORIENTED_EDGE ( 'NONE', *, *, #14838, .T. ) ;
#22224=ORIENTED_EDGE ( 'NONE', *, *, #11975, .T. ) ;
#22256=TOROIDAL_SURFACE ( 'NONE', #20396, 5.080000000000000071, 0.3810000000000000053 ) ;
#22289=VECTOR ( 'NONE', #17757, 1000.000000000000114 ) ;
#22352=DIRECTION ( 'NONE',  ( 0.000000000000000000, 1.000000000000000000, 0.000000000000000000 ) ) ;
#22368=ORIENTED_EDGE ( 'NONE', *, *, #3971, .T. ) ;
#22411=LINE ( 'NONE', #15510, #5418 ) ;
#22587=EDGE_CURVE ( 'NONE', #3605, #4945, #3328, .T. ) ;
#22679=EDGE_CURVE ( 'NONE', #19336, #2102, #16246, .T. ) ;
#22719=ORIENTED_EDGE ( 'NONE', *, *, #4003, .F. ) ;
#22799=CARTESIAN_POINT ( 'NONE',  ( -12.31899999999987827, -3576.167599999831964, 2247.391999999993914 ) ) ;
#22820=CIRCLE ( 'NONE', #4133, 5.460999999999938126 ) ;
#22835=DIRECTION ( 'NONE',  ( -2.326004358982014616E-14, 0.5000000000030029312, -0.8660254037827048723 ) ) ;
#22839=DIRECTION ( 'NONE',  ( -1.000000000000000000, 2.330758767201999921E-14, 2.356218894535000080E-14 ) ) ;
#22848=CARTESIAN_POINT ( 'NONE',  ( -12.69999999999997087, -3575.727659094874525, 2247.391999999782001 ) ) ;
#22876=ORIENTED_EDGE ( 'NONE', *, *, #4003, .T. ) ;
#22931=CARTESIAN_POINT ( 'NONE',  ( -12.31900000000000084, -3578.860000000000127, 2244.679313203000220 ) ) ;
#22960=LINE ( 'NONE', #7271, #20685 ) ;
#22983=DIRECTION ( 'NONE',  ( -1.000000000000000000, 2.330758767201999921E-14, 2.343004830739999973E-14 ) ) ;
#23062=CARTESIAN_POINT ( 'NONE',  ( -12.31900000000002748, -3580.206200000138779, 2245.060313203175610 ) ) ;
#23094=( NAMED_UNIT ( * ) SI_UNIT ( $, .STERADIAN. ) SOLID_ANGLE_UNIT ( ) );
#23151=PLANE ( 'NONE',  #69 ) ;
#23208=COLOUR_RGB('Black',0.12,0.14,0.17);
#23209=FILL_AREA_STYLE_COLOUR('',#23208);
#23210=FILL_AREA_STYLE('',(#23209));
#23211=SURFACE_STYLE_FILL_AREA(#23210);
#23212=SURFACE_SIDE_STYLE('',(#23211));
#23213=SURFACE_STYLE_USAGE(.BOTH.,#23212);
#23214=PRESENTATION_STYLE_ASSIGNMENT((#23213));
#23224=STYLED_ITEM('',(#23214),#13479);
#23237=MECHANICAL_DESIGN_GEOMETRIC_PRESENTATION_REPRESENTATION('',(#23224),#2257);
ENDSEC;
END-ISO-10303-21;
